ISO-10303-21;
HEADER;
/* Generated by software containing ST-Developer
 * from STEP Tools, Inc. (www.steptools.com) 
 */

FILE_DESCRIPTION(
/* description */ ('STEP AP214'),
/* implementation_level */ '2;1');

FILE_NAME(
/* name */ 'Pivot Pins 3.step',
/* time_stamp */ '2026-10-06T11:11:25-07:00',
/* author */ (''),
/* organization */ (''),
/* preprocessor_version */ 'ST-DEVELOPER v20.2',
/* originating_system */ 'Autodesk Translation Framework v15.15.0.0',
/* authorisation */ '');

FILE_SCHEMA (('AUTOMOTIVE_DESIGN { 1 0 10303 214 3 1 1 }'));
ENDSEC;

DATA;
#10=MECHANICAL_DESIGN_GEOMETRIC_PRESENTATION_REPRESENTATION('',(#700),#47717);
#676=SHAPE_REPRESENTATION_RELATIONSHIP('SRR','None',#47763,#688);
#688=ADVANCED_BREP_SHAPE_REPRESENTATION('',(#712),#47707);
#700=STYLED_ITEM('',(#47830),#712);
#712=MANIFOLD_SOLID_BREP('Body1',#8927);
#724=FACE_BOUND('',#2600,.T.);
#725=FACE_BOUND('',#2602,.T.);
#763=PLANE('',#9120);
#764=PLANE('',#9121);
#886=LINE('',#15682,#1373);
#1373=VECTOR('',#10053,2.);
#1860=CYLINDRICAL_SURFACE('',#9115,2.);
#2082=FACE_OUTER_BOUND('',#2596,.T.);
#2083=FACE_OUTER_BOUND('',#2597,.T.);
#2084=FACE_OUTER_BOUND('',#2598,.T.);
#2085=FACE_OUTER_BOUND('',#2599,.T.);
#2086=FACE_OUTER_BOUND('',#2601,.T.);
#2596=EDGE_LOOP('',(#5797));
#2597=EDGE_LOOP('',(#5798,#5799,#5800,#5801));
#2598=EDGE_LOOP('',(#5802));
#2599=EDGE_LOOP('',(#5803));
#2600=EDGE_LOOP('',(#5804));
#2601=EDGE_LOOP('',(#5805));
#2602=EDGE_LOOP('',(#5806));
#3150=CIRCLE('',#9114,3.30718913883074);
#3151=CIRCLE('',#9116,2.);
#3152=CIRCLE('',#9117,2.);
#3153=CIRCLE('',#9119,3.30718913883074);
#3554=VERTEX_POINT('',#15676);
#3555=VERTEX_POINT('',#15679);
#3556=VERTEX_POINT('',#15681);
#3557=VERTEX_POINT('',#15685);
#4424=EDGE_CURVE('',#3554,#3554,#3150,.T.);
#4425=EDGE_CURVE('',#3555,#3555,#3151,.T.);
#4426=EDGE_CURVE('',#3555,#3556,#886,.T.);
#4427=EDGE_CURVE('',#3556,#3556,#3152,.T.);
#4428=EDGE_CURVE('',#3557,#3557,#3153,.T.);
#5797=ORIENTED_EDGE('',*,*,#4424,.T.);
#5798=ORIENTED_EDGE('',*,*,#4425,.F.);
#5799=ORIENTED_EDGE('',*,*,#4426,.T.);
#5800=ORIENTED_EDGE('',*,*,#4427,.T.);
#5801=ORIENTED_EDGE('',*,*,#4426,.F.);
#5802=ORIENTED_EDGE('',*,*,#4428,.F.);
#5803=ORIENTED_EDGE('',*,*,#4428,.T.);
#5804=ORIENTED_EDGE('',*,*,#4427,.F.);
#5805=ORIENTED_EDGE('',*,*,#4424,.F.);
#5806=ORIENTED_EDGE('',*,*,#4425,.T.);
#8405=SPHERICAL_SURFACE('',#9113,4.);
#8406=SPHERICAL_SURFACE('',#9118,4.);
#8432=ADVANCED_FACE('',(#2082),#8405,.T.);
#8433=ADVANCED_FACE('',(#2083),#1860,.T.);
#8434=ADVANCED_FACE('',(#2084),#8406,.T.);
#8435=ADVANCED_FACE('',(#2085,#724),#763,.T.);
#8436=ADVANCED_FACE('',(#2086,#725),#764,.T.);
#8927=CLOSED_SHELL('',(#8432,#8433,#8434,#8435,#8436));
#9112=AXIS2_PLACEMENT_3D('',#15674,#10043,#10044);
#9113=AXIS2_PLACEMENT_3D('',#15675,#10045,#10046);
#9114=AXIS2_PLACEMENT_3D('',#15677,#10047,#10048);
#9115=AXIS2_PLACEMENT_3D('',#15678,#10049,#10050);
#9116=AXIS2_PLACEMENT_3D('',#15680,#10051,#10052);
#9117=AXIS2_PLACEMENT_3D('',#15683,#10054,#10055);
#9118=AXIS2_PLACEMENT_3D('',#15684,#10056,#10057);
#9119=AXIS2_PLACEMENT_3D('',#15686,#10058,#10059);
#9120=AXIS2_PLACEMENT_3D('',#15687,#10060,#10061);
#9121=AXIS2_PLACEMENT_3D('',#15688,#10062,#10063);
#10043=DIRECTION('axis',(0.,0.,1.));
#10044=DIRECTION('refdir',(1.,0.,0.));
#10045=DIRECTION('center_axis',(0.,-1.,0.));
#10046=DIRECTION('ref_axis',(1.,0.,0.));
#10047=DIRECTION('center_axis',(2.50063434304147E-17,1.27632226958495E-16,
1.));
#10048=DIRECTION('ref_axis',(3.19161530011276E-33,-1.,1.27632226958495E-16));
#10049=DIRECTION('center_axis',(2.50063434304147E-17,1.27632226958495E-16,
1.));
#10050=DIRECTION('ref_axis',(3.19161530011276E-33,-1.,1.27632226958495E-16));
#10051=DIRECTION('center_axis',(2.50063434304147E-17,1.27632226958495E-16,
1.));
#10052=DIRECTION('ref_axis',(3.19161530011276E-33,-1.,1.27632226958495E-16));
#10053=DIRECTION('',(-2.50063434304147E-17,-1.27632226958495E-16,-1.));
#10054=DIRECTION('center_axis',(2.50063434304147E-17,1.27632226958495E-16,
1.));
#10055=DIRECTION('ref_axis',(3.19161530011276E-33,-1.,1.27632226958495E-16));
#10056=DIRECTION('center_axis',(0.,1.,0.));
#10057=DIRECTION('ref_axis',(1.,0.,0.));
#10058=DIRECTION('center_axis',(2.50063434304147E-17,1.27632226958495E-16,
1.));
#10059=DIRECTION('ref_axis',(3.19161530011276E-33,-1.,1.27632226958495E-16));
#10060=DIRECTION('center_axis',(2.50063434304147E-17,1.27632226958495E-16,
1.));
#10061=DIRECTION('ref_axis',(2.50063434304147E-17,-1.,1.27632226958495E-16));
#10062=DIRECTION('center_axis',(-2.50063434304147E-17,-1.27632226958495E-16,
-1.));
#10063=DIRECTION('ref_axis',(2.50063434304147E-17,-1.,1.27632226958495E-16));
#15674=CARTESIAN_POINT('',(0.,0.,0.));
#15675=CARTESIAN_POINT('Origin',(-38.9776940652676,8.40516957928876,178.735485069079));
#15676=CARTESIAN_POINT('',(-42.2848832040984,8.40516957928876,180.985485069079));
#15677=CARTESIAN_POINT('Origin',(-38.9776940652676,8.40516957928876,180.985485069079));
#15678=CARTESIAN_POINT('Origin',(-38.9776940652676,8.40516957928876,175.985485069079));
#15679=CARTESIAN_POINT('',(-38.9776940652676,10.4051695792888,180.985485069079));
#15680=CARTESIAN_POINT('Origin',(-38.9776940652676,8.40516957928876,180.985485069079));
#15681=CARTESIAN_POINT('',(-38.9776940652676,10.4051695792888,170.985485069079));
#15682=CARTESIAN_POINT('',(-38.9776940652676,10.4051695792888,175.985485069079));
#15683=CARTESIAN_POINT('Origin',(-38.9776940652676,8.40516957928876,170.985485069079));
#15684=CARTESIAN_POINT('Origin',(-38.9776940652676,8.40516957928876,173.235485069079));
#15685=CARTESIAN_POINT('',(-42.2848832040984,8.40516957928876,170.985485069079));
#15686=CARTESIAN_POINT('Origin',(-38.9776940652676,8.40516957928876,170.985485069079));
#15687=CARTESIAN_POINT('Origin',(-36.9776940652676,8.40516957928876,170.985485069079));
#15688=CARTESIAN_POINT('Origin',(-36.9776940652676,8.40516957928876,180.985485069079));
#47693=UNCERTAINTY_MEASURE_WITH_UNIT(LENGTH_MEASURE(0.01),#47718,
'DISTANCE_ACCURACY_VALUE',
'Maximum model space distance between geometric entities at asserted c
onnectivities');
#47703=UNCERTAINTY_MEASURE_WITH_UNIT(LENGTH_MEASURE(0.01),#47718,
'DISTANCE_ACCURACY_VALUE',
'Maximum model space distance between geometric entities at asserted c
onnectivities');
#47707=(
GEOMETRIC_REPRESENTATION_CONTEXT(3)
GLOBAL_UNCERTAINTY_ASSIGNED_CONTEXT((#47693))
GLOBAL_UNIT_ASSIGNED_CONTEXT((#47718,#47720,#47721))
REPRESENTATION_CONTEXT('','3D')
);
#47717=(
GEOMETRIC_REPRESENTATION_CONTEXT(3)
GLOBAL_UNCERTAINTY_ASSIGNED_CONTEXT((#47703))
GLOBAL_UNIT_ASSIGNED_CONTEXT((#47718,#47720,#47721))
REPRESENTATION_CONTEXT('','3D')
);
#47718=(
LENGTH_UNIT()
NAMED_UNIT(*)
SI_UNIT(.MILLI.,.METRE.)
);
#47720=(
NAMED_UNIT(*)
PLANE_ANGLE_UNIT()
SI_UNIT($,.RADIAN.)
);
#47721=(
NAMED_UNIT(*)
SI_UNIT($,.STERADIAN.)
SOLID_ANGLE_UNIT()
);
#47725=SHAPE_DEFINITION_REPRESENTATION(#47738,#47763);
#47738=PRODUCT_DEFINITION_SHAPE('',$,#47777);
#47763=SHAPE_REPRESENTATION('',(#9112),#47707);
#47773=PRODUCT_DEFINITION_CONTEXT('part definition',#47814,'design');
#47777=PRODUCT_DEFINITION('Pivot Pins 3','Pivot Pins 3',#47790,#47773);
#47790=PRODUCT_DEFINITION_FORMATION('',$,#47819);
#47814=APPLICATION_CONTEXT(
'Core Data for Automotive Mechanical Design Process');
#47815=PRODUCT_CONTEXT('part definition',#47814,'mechanical');
#47819=PRODUCT('Pivot Pins 3','Pivot Pins 3',$,(#47815));
#47830=PRESENTATION_STYLE_ASSIGNMENT((#47832));
#47832=SURFACE_STYLE_USAGE(.BOTH.,#47834);
#47834=SURFACE_SIDE_STYLE('',(#47836));
#47836=SURFACE_STYLE_FILL_AREA(#47838);
#47838=FILL_AREA_STYLE('Opaque(202,209,238)',(#47840));
#47840=FILL_AREA_STYLE_COLOUR('Opaque(202,209,238)',#47842);
#47842=COLOUR_RGB('Opaque(202,209,238)', 0.66274510, 0.83137255, 0.94901961);
ENDSEC;
END-ISO-10303-21;
